ISO-10303-21;
HEADER;
/* Generated by software containing ST-Developer
 * from STEP Tools, Inc. (www.steptools.com) 
 */

FILE_DESCRIPTION(
/* description */ ('Rigid flange shaft coupling assembly'),
/* implementation_level */ '2;1');

FILE_NAME(
/* name */ 'M8x25 Bolt.step',
/* time_stamp */ '2026-10-27T10:47:16-07:00',
/* author */ (''),
/* organization */ (''),
/* preprocessor_version */ 'ST-DEVELOPER v20.2',
/* originating_system */ 'Autodesk Translation Framework v15.17.0.0',
/* authorisation */ '');

FILE_SCHEMA (('AUTOMOTIVE_DESIGN { 1 0 10303 214 3 1 1 }'));
ENDSEC;

DATA;
#10=MECHANICAL_DESIGN_GEOMETRIC_PRESENTATION_REPRESENTATION('',(#411),#9141);
#23=CONICAL_SURFACE('',#5296,0.625,0.785398163397448);
#24=CONICAL_SURFACE('',#5300,0.635,0.785398163397449);
#25=CONICAL_SURFACE('',#5304,0.41,0.463647609000806);
#38=ORIENTED_CLOSED_SHELL('',*,#4765,.F.);
#41=BREP_WITH_VOIDS('Body1',#4766,(#38));
#354=SHAPE_REPRESENTATION_RELATIONSHIP('SRR','None',#9289,#382);
#382=ADVANCED_BREP_SHAPE_REPRESENTATION('',(#41),#9124);
#411=STYLED_ITEM('',(#9507),#41);
#516=FACE_BOUND('',#1196,.T.);
#634=PLANE('',#5284);
#635=PLANE('',#5285);
#636=PLANE('',#5286);
#637=PLANE('',#5287);
#638=PLANE('',#5288);
#639=PLANE('',#5289);
#640=PLANE('',#5290);
#641=PLANE('',#5291);
#642=PLANE('',#5292);
#643=PLANE('',#5294);
#644=PLANE('',#5302);
#847=FACE_OUTER_BOUND('',#1182,.T.);
#848=FACE_OUTER_BOUND('',#1183,.T.);
#849=FACE_OUTER_BOUND('',#1184,.T.);
#850=FACE_OUTER_BOUND('',#1185,.T.);
#851=FACE_OUTER_BOUND('',#1186,.T.);
#852=FACE_OUTER_BOUND('',#1187,.T.);
#853=FACE_OUTER_BOUND('',#1188,.T.);
#854=FACE_OUTER_BOUND('',#1189,.T.);
#855=FACE_OUTER_BOUND('',#1190,.T.);
#856=FACE_OUTER_BOUND('',#1191,.T.);
#857=FACE_OUTER_BOUND('',#1192,.T.);
#858=FACE_OUTER_BOUND('',#1193,.T.);
#859=FACE_OUTER_BOUND('',#1194,.T.);
#860=FACE_OUTER_BOUND('',#1195,.T.);
#861=FACE_OUTER_BOUND('',#1197,.T.);
#862=FACE_OUTER_BOUND('',#1198,.T.);
#1182=EDGE_LOOP('',(#3707,#3708,#3709,#3710));
#1183=EDGE_LOOP('',(#3711,#3712,#3713,#3714));
#1184=EDGE_LOOP('',(#3715,#3716,#3717,#3718));
#1185=EDGE_LOOP('',(#3719,#3720,#3721,#3722));
#1186=EDGE_LOOP('',(#3723,#3724,#3725,#3726));
#1187=EDGE_LOOP('',(#3727,#3728,#3729,#3730));
#1188=EDGE_LOOP('',(#3731,#3732,#3733,#3734,#3735,#3736));
#1189=EDGE_LOOP('',(#3737,#3738,#3739,#3740,#3741,#3742));
#1190=EDGE_LOOP('',(#3743));
#1191=EDGE_LOOP('',(#3744));
#1192=EDGE_LOOP('',(#3745,#3746,#3747,#3748));
#1193=EDGE_LOOP('',(#3749,#3750,#3751,#3752));
#1194=EDGE_LOOP('',(#3753,#3754,#3755,#3756));
#1195=EDGE_LOOP('',(#3757));
#1196=EDGE_LOOP('',(#3758));
#1197=EDGE_LOOP('',(#3759,#3760,#3761,#3762));
#1198=EDGE_LOOP('',(#3763,#3764,#3765,#3766));
#1543=LINE('',#8011,#1888);
#1544=LINE('',#8013,#1889);
#1545=LINE('',#8015,#1890);
#1546=LINE('',#8016,#1891);
#1547=LINE('',#8019,#1892);
#1548=LINE('',#8021,#1893);
#1549=LINE('',#8022,#1894);
#1550=LINE('',#8025,#1895);
#1551=LINE('',#8027,#1896);
#1552=LINE('',#8028,#1897);
#1553=LINE('',#8031,#1898);
#1554=LINE('',#8033,#1899);
#1555=LINE('',#8034,#1900);
#1556=LINE('',#8037,#1901);
#1557=LINE('',#8039,#1902);
#1558=LINE('',#8040,#1903);
#1559=LINE('',#8042,#1904);
#1560=LINE('',#8043,#1905);
#1561=LINE('',#8055,#1906);
#1562=LINE('',#8059,#1907);
#1563=LINE('',#8063,#1908);
#1564=LINE('',#8070,#1909);
#1565=LINE('',#8072,#1910);
#1888=VECTOR('',#6164,1.);
#1889=VECTOR('',#6165,1.);
#1890=VECTOR('',#6166,1.);
#1891=VECTOR('',#6167,1.);
#1892=VECTOR('',#6170,1.);
#1893=VECTOR('',#6171,1.);
#1894=VECTOR('',#6172,1.);
#1895=VECTOR('',#6175,1.);
#1896=VECTOR('',#6176,1.);
#1897=VECTOR('',#6177,1.);
#1898=VECTOR('',#6180,1.);
#1899=VECTOR('',#6181,1.);
#1900=VECTOR('',#6182,1.);
#1901=VECTOR('',#6185,1.);
#1902=VECTOR('',#6186,1.);
#1903=VECTOR('',#6187,1.);
#1904=VECTOR('',#6190,1.);
#1905=VECTOR('',#6191,1.);
#1906=VECTOR('',#6208,0.625);
#1907=VECTOR('',#6213,0.65);
#1908=VECTOR('',#6218,0.635);
#1909=VECTOR('',#6227,0.41);
#1910=VECTOR('',#6230,0.4);
#2165=CIRCLE('',#5293,0.3933);
#2166=CIRCLE('',#5295,0.6);
#2167=CIRCLE('',#5297,0.65);
#2168=CIRCLE('',#5299,0.65);
#2169=CIRCLE('',#5301,0.62);
#2170=CIRCLE('',#5303,0.42);
#2171=CIRCLE('',#5305,0.3933);
#2438=VERTEX_POINT('',#8009);
#2439=VERTEX_POINT('',#8010);
#2440=VERTEX_POINT('',#8012);
#2441=VERTEX_POINT('',#8014);
#2442=VERTEX_POINT('',#8018);
#2443=VERTEX_POINT('',#8020);
#2444=VERTEX_POINT('',#8024);
#2445=VERTEX_POINT('',#8026);
#2446=VERTEX_POINT('',#8030);
#2447=VERTEX_POINT('',#8032);
#2448=VERTEX_POINT('',#8036);
#2449=VERTEX_POINT('',#8038);
#2450=VERTEX_POINT('',#8047);
#2451=VERTEX_POINT('',#8050);
#2452=VERTEX_POINT('',#8053);
#2453=VERTEX_POINT('',#8057);
#2454=VERTEX_POINT('',#8061);
#2455=VERTEX_POINT('',#8065);
#2456=VERTEX_POINT('',#8068);
#2897=EDGE_CURVE('',#2438,#2439,#1543,.T.);
#2898=EDGE_CURVE('',#2439,#2440,#1544,.T.);
#2899=EDGE_CURVE('',#2440,#2441,#1545,.T.);
#2900=EDGE_CURVE('',#2438,#2441,#1546,.T.);
#2901=EDGE_CURVE('',#2439,#2442,#1547,.T.);
#2902=EDGE_CURVE('',#2442,#2443,#1548,.T.);
#2903=EDGE_CURVE('',#2443,#2440,#1549,.T.);
#2904=EDGE_CURVE('',#2442,#2444,#1550,.T.);
#2905=EDGE_CURVE('',#2444,#2445,#1551,.T.);
#2906=EDGE_CURVE('',#2445,#2443,#1552,.T.);
#2907=EDGE_CURVE('',#2444,#2446,#1553,.T.);
#2908=EDGE_CURVE('',#2446,#2447,#1554,.T.);
#2909=EDGE_CURVE('',#2447,#2445,#1555,.T.);
#2910=EDGE_CURVE('',#2446,#2448,#1556,.T.);
#2911=EDGE_CURVE('',#2448,#2449,#1557,.T.);
#2912=EDGE_CURVE('',#2449,#2447,#1558,.T.);
#2913=EDGE_CURVE('',#2448,#2438,#1559,.T.);
#2914=EDGE_CURVE('',#2441,#2449,#1560,.T.);
#2915=EDGE_CURVE('',#2450,#2450,#2165,.T.);
#2916=EDGE_CURVE('',#2451,#2451,#2166,.T.);
#2917=EDGE_CURVE('',#2452,#2452,#2167,.T.);
#2918=EDGE_CURVE('',#2452,#2451,#1561,.T.);
#2919=EDGE_CURVE('',#2453,#2453,#2168,.T.);
#2920=EDGE_CURVE('',#2453,#2452,#1562,.T.);
#2921=EDGE_CURVE('',#2454,#2454,#2169,.T.);
#2922=EDGE_CURVE('',#2454,#2453,#1563,.T.);
#2923=EDGE_CURVE('',#2455,#2455,#2170,.T.);
#2924=EDGE_CURVE('',#2456,#2456,#2171,.F.);
#2925=EDGE_CURVE('',#2456,#2455,#1564,.T.);
#2926=EDGE_CURVE('',#2450,#2456,#1565,.T.);
#3707=ORIENTED_EDGE('',*,*,#2897,.T.);
#3708=ORIENTED_EDGE('',*,*,#2898,.T.);
#3709=ORIENTED_EDGE('',*,*,#2899,.T.);
#3710=ORIENTED_EDGE('',*,*,#2900,.F.);
#3711=ORIENTED_EDGE('',*,*,#2901,.T.);
#3712=ORIENTED_EDGE('',*,*,#2902,.T.);
#3713=ORIENTED_EDGE('',*,*,#2903,.T.);
#3714=ORIENTED_EDGE('',*,*,#2898,.F.);
#3715=ORIENTED_EDGE('',*,*,#2904,.T.);
#3716=ORIENTED_EDGE('',*,*,#2905,.T.);
#3717=ORIENTED_EDGE('',*,*,#2906,.T.);
#3718=ORIENTED_EDGE('',*,*,#2902,.F.);
#3719=ORIENTED_EDGE('',*,*,#2907,.T.);
#3720=ORIENTED_EDGE('',*,*,#2908,.T.);
#3721=ORIENTED_EDGE('',*,*,#2909,.T.);
#3722=ORIENTED_EDGE('',*,*,#2905,.F.);
#3723=ORIENTED_EDGE('',*,*,#2910,.T.);
#3724=ORIENTED_EDGE('',*,*,#2911,.T.);
#3725=ORIENTED_EDGE('',*,*,#2912,.T.);
#3726=ORIENTED_EDGE('',*,*,#2908,.F.);
#3727=ORIENTED_EDGE('',*,*,#2913,.T.);
#3728=ORIENTED_EDGE('',*,*,#2900,.T.);
#3729=ORIENTED_EDGE('',*,*,#2914,.T.);
#3730=ORIENTED_EDGE('',*,*,#2911,.F.);
#3731=ORIENTED_EDGE('',*,*,#2913,.F.);
#3732=ORIENTED_EDGE('',*,*,#2910,.F.);
#3733=ORIENTED_EDGE('',*,*,#2907,.F.);
#3734=ORIENTED_EDGE('',*,*,#2904,.F.);
#3735=ORIENTED_EDGE('',*,*,#2901,.F.);
#3736=ORIENTED_EDGE('',*,*,#2897,.F.);
#3737=ORIENTED_EDGE('',*,*,#2914,.F.);
#3738=ORIENTED_EDGE('',*,*,#2899,.F.);
#3739=ORIENTED_EDGE('',*,*,#2903,.F.);
#3740=ORIENTED_EDGE('',*,*,#2906,.F.);
#3741=ORIENTED_EDGE('',*,*,#2909,.F.);
#3742=ORIENTED_EDGE('',*,*,#2912,.F.);
#3743=ORIENTED_EDGE('',*,*,#2915,.F.);
#3744=ORIENTED_EDGE('',*,*,#2916,.F.);
#3745=ORIENTED_EDGE('',*,*,#2917,.F.);
#3746=ORIENTED_EDGE('',*,*,#2918,.T.);
#3747=ORIENTED_EDGE('',*,*,#2916,.T.);
#3748=ORIENTED_EDGE('',*,*,#2918,.F.);
#3749=ORIENTED_EDGE('',*,*,#2919,.F.);
#3750=ORIENTED_EDGE('',*,*,#2920,.T.);
#3751=ORIENTED_EDGE('',*,*,#2917,.T.);
#3752=ORIENTED_EDGE('',*,*,#2920,.F.);
#3753=ORIENTED_EDGE('',*,*,#2921,.F.);
#3754=ORIENTED_EDGE('',*,*,#2922,.T.);
#3755=ORIENTED_EDGE('',*,*,#2919,.T.);
#3756=ORIENTED_EDGE('',*,*,#2922,.F.);
#3757=ORIENTED_EDGE('',*,*,#2921,.T.);
#3758=ORIENTED_EDGE('',*,*,#2923,.F.);
#3759=ORIENTED_EDGE('',*,*,#2924,.F.);
#3760=ORIENTED_EDGE('',*,*,#2925,.T.);
#3761=ORIENTED_EDGE('',*,*,#2923,.T.);
#3762=ORIENTED_EDGE('',*,*,#2925,.F.);
#3763=ORIENTED_EDGE('',*,*,#2915,.T.);
#3764=ORIENTED_EDGE('',*,*,#2926,.T.);
#3765=ORIENTED_EDGE('',*,*,#2924,.T.);
#3766=ORIENTED_EDGE('',*,*,#2926,.F.);
#4436=CYLINDRICAL_SURFACE('',#5298,0.65);
#4437=CYLINDRICAL_SURFACE('',#5306,0.3933);
#4583=ADVANCED_FACE('',(#847),#634,.F.);
#4584=ADVANCED_FACE('',(#848),#635,.F.);
#4585=ADVANCED_FACE('',(#849),#636,.F.);
#4586=ADVANCED_FACE('',(#850),#637,.F.);
#4587=ADVANCED_FACE('',(#851),#638,.F.);
#4588=ADVANCED_FACE('',(#852),#639,.F.);
#4589=ADVANCED_FACE('',(#853),#640,.F.);
#4590=ADVANCED_FACE('',(#854),#641,.F.);
#4591=ADVANCED_FACE('',(#855),#642,.F.);
#4592=ADVANCED_FACE('',(#856),#643,.T.);
#4593=ADVANCED_FACE('',(#857),#23,.T.);
#4594=ADVANCED_FACE('',(#858),#4436,.T.);
#4595=ADVANCED_FACE('',(#859),#24,.T.);
#4596=ADVANCED_FACE('',(#860,#516),#644,.T.);
#4597=ADVANCED_FACE('',(#861),#25,.T.);
#4598=ADVANCED_FACE('',(#862),#4437,.T.);
#4765=CLOSED_SHELL('',(#4583,#4584,#4585,#4586,#4587,#4588,#4589,#4590));
#4766=CLOSED_SHELL('',(#4591,#4592,#4593,#4594,#4595,#4596,#4597,#4598));
#5283=AXIS2_PLACEMENT_3D('',#8007,#6160,#6161);
#5284=AXIS2_PLACEMENT_3D('',#8008,#6162,#6163);
#5285=AXIS2_PLACEMENT_3D('',#8017,#6168,#6169);
#5286=AXIS2_PLACEMENT_3D('',#8023,#6173,#6174);
#5287=AXIS2_PLACEMENT_3D('',#8029,#6178,#6179);
#5288=AXIS2_PLACEMENT_3D('',#8035,#6183,#6184);
#5289=AXIS2_PLACEMENT_3D('',#8041,#6188,#6189);
#5290=AXIS2_PLACEMENT_3D('',#8044,#6192,#6193);
#5291=AXIS2_PLACEMENT_3D('',#8045,#6194,#6195);
#5292=AXIS2_PLACEMENT_3D('',#8046,#6196,#6197);
#5293=AXIS2_PLACEMENT_3D('',#8048,#6198,#6199);
#5294=AXIS2_PLACEMENT_3D('',#8049,#6200,#6201);
#5295=AXIS2_PLACEMENT_3D('',#8051,#6202,#6203);
#5296=AXIS2_PLACEMENT_3D('',#8052,#6204,#6205);
#5297=AXIS2_PLACEMENT_3D('',#8054,#6206,#6207);
#5298=AXIS2_PLACEMENT_3D('',#8056,#6209,#6210);
#5299=AXIS2_PLACEMENT_3D('',#8058,#6211,#6212);
#5300=AXIS2_PLACEMENT_3D('',#8060,#6214,#6215);
#5301=AXIS2_PLACEMENT_3D('',#8062,#6216,#6217);
#5302=AXIS2_PLACEMENT_3D('',#8064,#6219,#6220);
#5303=AXIS2_PLACEMENT_3D('',#8066,#6221,#6222);
#5304=AXIS2_PLACEMENT_3D('',#8067,#6223,#6224);
#5305=AXIS2_PLACEMENT_3D('',#8069,#6225,#6226);
#5306=AXIS2_PLACEMENT_3D('',#8071,#6228,#6229);
#6160=DIRECTION('axis',(0.,0.,1.));
#6161=DIRECTION('refdir',(1.,0.,0.));
#6162=DIRECTION('center_axis',(0.866025403784439,0.,-0.5));
#6163=DIRECTION('ref_axis',(0.5,0.,0.866025403784439));
#6164=DIRECTION('',(-0.5,0.,-0.866025403784439));
#6165=DIRECTION('',(0.,-1.,0.));
#6166=DIRECTION('',(0.5,0.,0.866025403784439));
#6167=DIRECTION('',(0.,-1.,0.));
#6168=DIRECTION('center_axis',(1.60246890531964E-16,0.,-1.));
#6169=DIRECTION('ref_axis',(1.,0.,1.60246890531964E-16));
#6170=DIRECTION('',(-1.,0.,-1.60246890531964E-16));
#6171=DIRECTION('',(0.,-1.,0.));
#6172=DIRECTION('',(1.,0.,1.60246890531964E-16));
#6173=DIRECTION('center_axis',(-0.866025403784439,0.,-0.5));
#6174=DIRECTION('ref_axis',(0.5,0.,-0.866025403784439));
#6175=DIRECTION('',(-0.5,0.,0.866025403784439));
#6176=DIRECTION('',(0.,-1.,0.));
#6177=DIRECTION('',(0.5,0.,-0.866025403784439));
#6178=DIRECTION('center_axis',(-0.866025403784439,0.,0.5));
#6179=DIRECTION('ref_axis',(-0.5,0.,-0.866025403784439));
#6180=DIRECTION('',(0.5,0.,0.866025403784439));
#6181=DIRECTION('',(0.,-1.,0.));
#6182=DIRECTION('',(-0.5,0.,-0.866025403784439));
#6183=DIRECTION('center_axis',(-1.60246890531964E-16,0.,1.));
#6184=DIRECTION('ref_axis',(-1.,0.,-1.60246890531964E-16));
#6185=DIRECTION('',(1.,0.,1.60246890531964E-16));
#6186=DIRECTION('',(0.,-1.,0.));
#6187=DIRECTION('',(-1.,0.,-1.60246890531964E-16));
#6188=DIRECTION('center_axis',(0.866025403784439,0.,0.5));
#6189=DIRECTION('ref_axis',(-0.5,0.,0.866025403784439));
#6190=DIRECTION('',(0.5,0.,-0.866025403784439));
#6191=DIRECTION('',(-0.5,0.,0.866025403784439));
#6192=DIRECTION('center_axis',(0.,1.,0.));
#6193=DIRECTION('ref_axis',(1.,0.,0.));
#6194=DIRECTION('center_axis',(0.,-1.,0.));
#6195=DIRECTION('ref_axis',(0.,0.,-1.));
#6196=DIRECTION('center_axis',(0.,1.,0.));
#6197=DIRECTION('ref_axis',(1.,0.,0.));
#6198=DIRECTION('center_axis',(0.,1.,0.));
#6199=DIRECTION('ref_axis',(1.,0.,0.));
#6200=DIRECTION('center_axis',(0.,1.,0.));
#6201=DIRECTION('ref_axis',(0.,0.,1.));
#6202=DIRECTION('center_axis',(0.,-1.,0.));
#6203=DIRECTION('ref_axis',(1.,0.,0.));
#6204=DIRECTION('center_axis',(0.,-1.,0.));
#6205=DIRECTION('ref_axis',(1.,0.,0.));
#6206=DIRECTION('center_axis',(0.,-1.,0.));
#6207=DIRECTION('ref_axis',(1.,0.,0.));
#6208=DIRECTION('',(0.707106781186548,0.707106781186547,8.65956056235493E-17));
#6209=DIRECTION('center_axis',(0.,-1.,0.));
#6210=DIRECTION('ref_axis',(1.,0.,0.));
#6211=DIRECTION('center_axis',(0.,-1.,0.));
#6212=DIRECTION('ref_axis',(1.,0.,0.));
#6213=DIRECTION('',(0.,1.,0.));
#6214=DIRECTION('center_axis',(0.,1.,0.));
#6215=DIRECTION('ref_axis',(1.,0.,0.));
#6216=DIRECTION('center_axis',(0.,-1.,0.));
#6217=DIRECTION('ref_axis',(1.,0.,0.));
#6218=DIRECTION('',(-0.707106781186548,0.707106781186547,-8.65956056235494E-17));
#6219=DIRECTION('center_axis',(0.,-1.,0.));
#6220=DIRECTION('ref_axis',(0.,0.,-1.));
#6221=DIRECTION('center_axis',(0.,-1.,0.));
#6222=DIRECTION('ref_axis',(1.,0.,0.));
#6223=DIRECTION('center_axis',(0.,1.,0.));
#6224=DIRECTION('ref_axis',(1.,0.,0.));
#6225=DIRECTION('center_axis',(0.,1.,0.));
#6226=DIRECTION('ref_axis',(1.,0.,0.));
#6227=DIRECTION('',(-0.447213595499958,0.894427190999916,-5.47678698264203E-17));
#6228=DIRECTION('center_axis',(0.,-1.,0.));
#6229=DIRECTION('ref_axis',(1.,0.,0.));
#6230=DIRECTION('',(0.,1.,0.));
#8007=CARTESIAN_POINT('',(0.,0.,0.));
#8008=CARTESIAN_POINT('Origin',(0.173205080756888,-0.8,-0.3));
#8009=CARTESIAN_POINT('',(0.346410161513775,-0.8,0.));
#8010=CARTESIAN_POINT('',(0.173205080756888,-0.8,-0.3));
#8011=CARTESIAN_POINT('',(0.346410161513775,-0.8,0.));
#8012=CARTESIAN_POINT('',(0.173205080756888,-1.28,-0.3));
#8013=CARTESIAN_POINT('',(0.173205080756888,-0.8,-0.3));
#8014=CARTESIAN_POINT('',(0.346410161513775,-1.28,0.));
#8015=CARTESIAN_POINT('',(0.346410161513775,-1.28,0.));
#8016=CARTESIAN_POINT('',(0.346410161513775,-0.8,0.));
#8017=CARTESIAN_POINT('Origin',(-0.173205080756888,-0.8,-0.3));
#8018=CARTESIAN_POINT('',(-0.173205080756888,-0.8,-0.3));
#8019=CARTESIAN_POINT('',(0.173205080756888,-0.8,-0.3));
#8020=CARTESIAN_POINT('',(-0.173205080756888,-1.28,-0.3));
#8021=CARTESIAN_POINT('',(-0.173205080756888,-0.8,-0.3));
#8022=CARTESIAN_POINT('',(0.173205080756888,-1.28,-0.3));
#8023=CARTESIAN_POINT('Origin',(-0.346410161513775,-0.8,-5.55111512312578E-17));
#8024=CARTESIAN_POINT('',(-0.346410161513775,-0.8,-4.24230095489963E-17));
#8025=CARTESIAN_POINT('',(-0.173205080756888,-0.8,-0.3));
#8026=CARTESIAN_POINT('',(-0.346410161513775,-1.28,-5.55111512312578E-17));
#8027=CARTESIAN_POINT('',(-0.346410161513775,-0.8,-4.24230095489963E-17));
#8028=CARTESIAN_POINT('',(-0.173205080756888,-1.28,-0.3));
#8029=CARTESIAN_POINT('Origin',(-0.173205080756888,-0.8,0.3));
#8030=CARTESIAN_POINT('',(-0.173205080756888,-0.8,0.3));
#8031=CARTESIAN_POINT('',(-0.346410161513775,-0.8,-4.24230095489963E-17));
#8032=CARTESIAN_POINT('',(-0.173205080756888,-1.28,0.3));
#8033=CARTESIAN_POINT('',(-0.173205080756888,-0.8,0.3));
#8034=CARTESIAN_POINT('',(-0.346410161513775,-1.28,-4.24230095489963E-17));
#8035=CARTESIAN_POINT('Origin',(0.173205080756888,-0.8,0.3));
#8036=CARTESIAN_POINT('',(0.173205080756888,-0.8,0.3));
#8037=CARTESIAN_POINT('',(-0.173205080756888,-0.8,0.3));
#8038=CARTESIAN_POINT('',(0.173205080756888,-1.28,0.3));
#8039=CARTESIAN_POINT('',(0.173205080756888,-0.8,0.3));
#8040=CARTESIAN_POINT('',(-0.173205080756888,-1.28,0.3));
#8041=CARTESIAN_POINT('Origin',(0.346410161513775,-0.8,0.));
#8042=CARTESIAN_POINT('',(0.173205080756888,-0.8,0.3));
#8043=CARTESIAN_POINT('',(0.173205080756888,-1.28,0.3));
#8044=CARTESIAN_POINT('Origin',(0.,-0.8,-5.55111512312578E-17));
#8045=CARTESIAN_POINT('Origin',(0.,-1.28,-5.55111512312578E-17));
#8046=CARTESIAN_POINT('Origin',(0.,-2.5,0.));
#8047=CARTESIAN_POINT('',(-0.3933,-2.5,4.81653586104654E-17));
#8048=CARTESIAN_POINT('Origin',(0.,-2.5,0.));
#8049=CARTESIAN_POINT('Origin',(0.6,0.8,0.));
#8050=CARTESIAN_POINT('',(-0.6,0.8,-7.34788079488412E-17));
#8051=CARTESIAN_POINT('Origin',(0.,0.8,0.));
#8052=CARTESIAN_POINT('Origin',(0.,0.775,0.));
#8053=CARTESIAN_POINT('',(-0.65,0.75,-7.9602041944578E-17));
#8054=CARTESIAN_POINT('Origin',(0.,0.75,0.));
#8055=CARTESIAN_POINT('',(-0.625,0.775,-7.65404249467096E-17));
#8056=CARTESIAN_POINT('Origin',(0.,0.39,0.));
#8057=CARTESIAN_POINT('',(-0.65,0.0299999999999998,-7.9602041944578E-17));
#8058=CARTESIAN_POINT('Origin',(0.,0.0299999999999998,0.));
#8059=CARTESIAN_POINT('',(-0.65,0.39,-7.9602041944578E-17));
#8060=CARTESIAN_POINT('Origin',(0.,0.0150000000000001,0.));
#8061=CARTESIAN_POINT('',(-0.62,5.89805981832114E-17,-7.59281015471359E-17));
#8062=CARTESIAN_POINT('Origin',(0.,0.,0.));
#8063=CARTESIAN_POINT('',(-0.635,0.0150000000000001,-7.77650717458569E-17));
#8064=CARTESIAN_POINT('Origin',(0.42,0.,0.));
#8065=CARTESIAN_POINT('',(-0.42,-3.46944695195361E-18,-5.14351655641888E-17));
#8066=CARTESIAN_POINT('Origin',(0.,0.,0.));
#8067=CARTESIAN_POINT('Origin',(0.,-0.02,0.));
#8068=CARTESIAN_POINT('',(-0.3933,-0.0534000000000001,4.81653586104654E-17));
#8069=CARTESIAN_POINT('Origin',(0.,-0.0534000000000001,0.));
#8070=CARTESIAN_POINT('',(-0.41,-0.02,-5.02105187650415E-17));
#8071=CARTESIAN_POINT('Origin',(0.,-1.48,0.));
#8072=CARTESIAN_POINT('',(-0.3933,-1.48,-4.81653586104654E-17));
#9091=UNCERTAINTY_MEASURE_WITH_UNIT(LENGTH_MEASURE(0.001),#9142,
'DISTANCE_ACCURACY_VALUE',
'Maximum model space distance between geometric entities at asserted c
onnectivities');
#9108=UNCERTAINTY_MEASURE_WITH_UNIT(LENGTH_MEASURE(0.001),#9142,
'DISTANCE_ACCURACY_VALUE',
'Maximum model space distance between geometric entities at asserted c
onnectivities');
#9124=(
GEOMETRIC_REPRESENTATION_CONTEXT(3)
GLOBAL_UNCERTAINTY_ASSIGNED_CONTEXT((#9091))
GLOBAL_UNIT_ASSIGNED_CONTEXT((#9142,#9144,#9145))
REPRESENTATION_CONTEXT('','3D')
);
#9141=(
GEOMETRIC_REPRESENTATION_CONTEXT(3)
GLOBAL_UNCERTAINTY_ASSIGNED_CONTEXT((#9108))
GLOBAL_UNIT_ASSIGNED_CONTEXT((#9142,#9144,#9145))
REPRESENTATION_CONTEXT('','3D')
);
#9142=(
LENGTH_UNIT()
NAMED_UNIT(*)
SI_UNIT(.CENTI.,.METRE.)
);
#9144=(
NAMED_UNIT(*)
PLANE_ANGLE_UNIT()
SI_UNIT($,.RADIAN.)
);
#9145=(
NAMED_UNIT(*)
SI_UNIT($,.STERADIAN.)
SOLID_ANGLE_UNIT()
);
#9161=SHAPE_DEFINITION_REPRESENTATION(#9195,#9289);
#9195=PRODUCT_DEFINITION_SHAPE('',$,#9322);
#9289=SHAPE_REPRESENTATION('',(#5283),#9124);
#9306=PRODUCT_DEFINITION_CONTEXT('part definition',#9404,'design');
#9322=PRODUCT_DEFINITION('M8x25 Bolt','M8x25 Bolt',#9354,#9306);
#9354=PRODUCT_DEFINITION_FORMATION('',$,#9421);
#9404=APPLICATION_CONTEXT(
'Core Data for Automotive Mechanical Design Process');
#9405=PRODUCT_CONTEXT('part definition',#9404,'mechanical');
#9421=PRODUCT('M8x25 Bolt','M8x25 Bolt','M8x25 Bolt',(#9405));
#9501=COLOUR_RGB('Black',0.12,0.14,0.17);
#9502=FILL_AREA_STYLE_COLOUR('',#9501);
#9503=FILL_AREA_STYLE('',(#9502));
#9504=SURFACE_STYLE_FILL_AREA(#9503);
#9505=SURFACE_SIDE_STYLE('',(#9504));
#9506=SURFACE_STYLE_USAGE(.BOTH.,#9505);
#9507=PRESENTATION_STYLE_ASSIGNMENT((#9506));
ENDSEC;
END-ISO-10303-21;
